ISO-10303-21;
HEADER;
/* Generated by software containing ST-Developer
 * from STEP Tools, Inc. (www.steptools.com) 
 */

FILE_DESCRIPTION(
/* description */ ('PAT-091'),
/* implementation_level */ '2;1');

FILE_NAME(
/* name */ 'Sliding pivot crosshead (1).step',
/* time_stamp */ '2026-10-27T15:34:44-07:00',
/* author */ (''),
/* organization */ (''),
/* preprocessor_version */ 'ST-DEVELOPER v20.2',
/* originating_system */ 'Autodesk Translation Framework v15.17.0.0',
/* authorisation */ '');

FILE_SCHEMA (('AUTOMOTIVE_DESIGN { 1 0 10303 214 3 1 1 }'));
ENDSEC;

DATA;
#10=MECHANICAL_DESIGN_GEOMETRIC_PRESENTATION_REPRESENTATION('',(#1016),#25100);
#699=B_SPLINE_CURVE_WITH_KNOTS('',3,(#22695,#22696,#22697,#22698,#22699,
#22700,#22701,#22702,#22703,#22704,#22705,#22706,#22707,#22708),
 .UNSPECIFIED.,.F.,.F.,(4,2,2,2,2,2,4),(0.598759558597949,0.624973342427788,
0.68746316342614,0.749952984424493,0.812442805422846,0.874932626421198,
0.901146410251035),.UNSPECIFIED.);
#700=B_SPLINE_CURVE_WITH_KNOTS('',3,(#22716,#22717,#22718,#22719,#22720,
#22721,#22722,#22723,#22724,#22725,#22726,#22727,#22728,#22729),
 .UNSPECIFIED.,.F.,.F.,(4,2,2,2,2,2,4),(0.0987909023149571,0.125004686144792,
0.187494507143145,0.249984328141498,0.31247414913985,0.374963970138203,
0.401177753968041),.UNSPECIFIED.);
#796=SHAPE_REPRESENTATION_RELATIONSHIP('SRR','None',#25560,#906);
#906=ADVANCED_BREP_SHAPE_REPRESENTATION('',(#1138),#25030);
#1016=STYLED_ITEM('',(#26205),#1138);
#1138=MANIFOLD_SOLID_BREP('Body1',#13295);
#1454=FACE_BOUND('',#3495,.T.);
#1455=FACE_BOUND('',#3497,.T.);
#1456=FACE_BOUND('',#3499,.T.);
#1457=FACE_BOUND('',#3501,.T.);
#1845=PLANE('',#15334);
#1846=PLANE('',#15340);
#1847=PLANE('',#15344);
#1848=PLANE('',#15345);
#1849=PLANE('',#15346);
#1850=PLANE('',#15347);
#1851=PLANE('',#15348);
#1852=PLANE('',#15349);
#2434=FACE_OUTER_BOUND('',#3491,.T.);
#2435=FACE_OUTER_BOUND('',#3492,.T.);
#2436=FACE_OUTER_BOUND('',#3493,.T.);
#2437=FACE_OUTER_BOUND('',#3494,.T.);
#2438=FACE_OUTER_BOUND('',#3496,.T.);
#2439=FACE_OUTER_BOUND('',#3498,.T.);
#2440=FACE_OUTER_BOUND('',#3500,.T.);
#2441=FACE_OUTER_BOUND('',#3502,.T.);
#2442=FACE_OUTER_BOUND('',#3503,.T.);
#2443=FACE_OUTER_BOUND('',#3504,.T.);
#3491=EDGE_LOOP('',(#10494,#10495));
#3492=EDGE_LOOP('',(#10496,#10497,#10498,#10499,#10500,#10501,#10502,#10503));
#3493=EDGE_LOOP('',(#10504,#10505,#10506));
#3494=EDGE_LOOP('',(#10507,#10508,#10509,#10510));
#3495=EDGE_LOOP('',(#10511,#10512,#10513,#10514));
#3496=EDGE_LOOP('',(#10515,#10516,#10517,#10518));
#3497=EDGE_LOOP('',(#10519));
#3498=EDGE_LOOP('',(#10520,#10521,#10522,#10523));
#3499=EDGE_LOOP('',(#10524));
#3500=EDGE_LOOP('',(#10525,#10526,#10527,#10528));
#3501=EDGE_LOOP('',(#10529));
#3502=EDGE_LOOP('',(#10530,#10531,#10532,#10533));
#3503=EDGE_LOOP('',(#10534,#10535,#10536,#10537));
#3504=EDGE_LOOP('',(#10538,#10539,#10540,#10541));
#4556=LINE('',#22691,#5296);
#4557=LINE('',#22712,#5297);
#4558=LINE('',#22731,#5298);
#4559=LINE('',#22736,#5299);
#4560=LINE('',#22741,#5300);
#4561=LINE('',#22743,#5301);
#4562=LINE('',#22745,#5302);
#4563=LINE('',#22746,#5303);
#4564=LINE('',#22749,#5304);
#4565=LINE('',#22751,#5305);
#4566=LINE('',#22752,#5306);
#4567=LINE('',#22755,#5307);
#4568=LINE('',#22757,#5308);
#4569=LINE('',#22758,#5309);
#4570=LINE('',#22760,#5310);
#4571=LINE('',#22761,#5311);
#5296=VECTOR('',#18400,1.);
#5297=VECTOR('',#18407,0.164999999999999);
#5298=VECTOR('',#18414,1.);
#5299=VECTOR('',#18419,0.604999999999997);
#5300=VECTOR('',#18424,1.);
#5301=VECTOR('',#18425,1.);
#5302=VECTOR('',#18426,1.);
#5303=VECTOR('',#18427,1.);
#5304=VECTOR('',#18430,1.);
#5305=VECTOR('',#18431,1.);
#5306=VECTOR('',#18432,1.);
#5307=VECTOR('',#18435,1.);
#5308=VECTOR('',#18436,1.);
#5309=VECTOR('',#18437,1.);
#5310=VECTOR('',#18440,1.);
#5311=VECTOR('',#18441,1.);
#5931=CIRCLE('',#15335,0.164999999999999);
#5932=CIRCLE('',#15337,0.164999999999999);
#5933=CIRCLE('',#15338,0.164999999999999);
#5934=CIRCLE('',#15339,0.164999999999999);
#5935=CIRCLE('',#15342,0.604999999999997);
#5936=CIRCLE('',#15343,0.604999999999997);
#6888=VERTEX_POINT('',#22689);
#6889=VERTEX_POINT('',#22690);
#6890=VERTEX_POINT('',#22694);
#6891=VERTEX_POINT('',#22709);
#6892=VERTEX_POINT('',#22711);
#6893=VERTEX_POINT('',#22714);
#6894=VERTEX_POINT('',#22733);
#6895=VERTEX_POINT('',#22735);
#6896=VERTEX_POINT('',#22739);
#6897=VERTEX_POINT('',#22740);
#6898=VERTEX_POINT('',#22742);
#6899=VERTEX_POINT('',#22744);
#6900=VERTEX_POINT('',#22748);
#6901=VERTEX_POINT('',#22750);
#6902=VERTEX_POINT('',#22754);
#6903=VERTEX_POINT('',#22756);
#8182=EDGE_CURVE('',#6888,#6889,#4556,.T.);
#8183=EDGE_CURVE('',#6888,#6889,#5931,.T.);
#8184=EDGE_CURVE('',#6890,#6888,#699,.T.);
#8185=EDGE_CURVE('',#6891,#6890,#5932,.T.);
#8186=EDGE_CURVE('',#6891,#6892,#4557,.T.);
#8187=EDGE_CURVE('',#6892,#6892,#5933,.T.);
#8188=EDGE_CURVE('',#6893,#6891,#5934,.T.);
#8189=EDGE_CURVE('',#6889,#6893,#700,.T.);
#8190=EDGE_CURVE('',#6893,#6890,#4558,.T.);
#8191=EDGE_CURVE('',#6894,#6894,#5935,.T.);
#8192=EDGE_CURVE('',#6894,#6895,#4559,.T.);
#8193=EDGE_CURVE('',#6895,#6895,#5936,.T.);
#8194=EDGE_CURVE('',#6896,#6897,#4560,.T.);
#8195=EDGE_CURVE('',#6897,#6898,#4561,.T.);
#8196=EDGE_CURVE('',#6899,#6898,#4562,.T.);
#8197=EDGE_CURVE('',#6896,#6899,#4563,.T.);
#8198=EDGE_CURVE('',#6900,#6896,#4564,.T.);
#8199=EDGE_CURVE('',#6901,#6899,#4565,.T.);
#8200=EDGE_CURVE('',#6900,#6901,#4566,.T.);
#8201=EDGE_CURVE('',#6902,#6900,#4567,.T.);
#8202=EDGE_CURVE('',#6903,#6901,#4568,.T.);
#8203=EDGE_CURVE('',#6902,#6903,#4569,.T.);
#8204=EDGE_CURVE('',#6897,#6902,#4570,.T.);
#8205=EDGE_CURVE('',#6898,#6903,#4571,.T.);
#10494=ORIENTED_EDGE('',*,*,#8182,.F.);
#10495=ORIENTED_EDGE('',*,*,#8183,.T.);
#10496=ORIENTED_EDGE('',*,*,#8184,.F.);
#10497=ORIENTED_EDGE('',*,*,#8185,.F.);
#10498=ORIENTED_EDGE('',*,*,#8186,.T.);
#10499=ORIENTED_EDGE('',*,*,#8187,.F.);
#10500=ORIENTED_EDGE('',*,*,#8186,.F.);
#10501=ORIENTED_EDGE('',*,*,#8188,.F.);
#10502=ORIENTED_EDGE('',*,*,#8189,.F.);
#10503=ORIENTED_EDGE('',*,*,#8183,.F.);
#10504=ORIENTED_EDGE('',*,*,#8190,.F.);
#10505=ORIENTED_EDGE('',*,*,#8188,.T.);
#10506=ORIENTED_EDGE('',*,*,#8185,.T.);
#10507=ORIENTED_EDGE('',*,*,#8191,.F.);
#10508=ORIENTED_EDGE('',*,*,#8192,.T.);
#10509=ORIENTED_EDGE('',*,*,#8193,.F.);
#10510=ORIENTED_EDGE('',*,*,#8192,.F.);
#10511=ORIENTED_EDGE('',*,*,#8189,.T.);
#10512=ORIENTED_EDGE('',*,*,#8190,.T.);
#10513=ORIENTED_EDGE('',*,*,#8184,.T.);
#10514=ORIENTED_EDGE('',*,*,#8182,.T.);
#10515=ORIENTED_EDGE('',*,*,#8194,.T.);
#10516=ORIENTED_EDGE('',*,*,#8195,.T.);
#10517=ORIENTED_EDGE('',*,*,#8196,.F.);
#10518=ORIENTED_EDGE('',*,*,#8197,.F.);
#10519=ORIENTED_EDGE('',*,*,#8193,.T.);
#10520=ORIENTED_EDGE('',*,*,#8198,.T.);
#10521=ORIENTED_EDGE('',*,*,#8197,.T.);
#10522=ORIENTED_EDGE('',*,*,#8199,.F.);
#10523=ORIENTED_EDGE('',*,*,#8200,.F.);
#10524=ORIENTED_EDGE('',*,*,#8187,.T.);
#10525=ORIENTED_EDGE('',*,*,#8201,.T.);
#10526=ORIENTED_EDGE('',*,*,#8200,.T.);
#10527=ORIENTED_EDGE('',*,*,#8202,.F.);
#10528=ORIENTED_EDGE('',*,*,#8203,.F.);
#10529=ORIENTED_EDGE('',*,*,#8191,.T.);
#10530=ORIENTED_EDGE('',*,*,#8204,.T.);
#10531=ORIENTED_EDGE('',*,*,#8203,.T.);
#10532=ORIENTED_EDGE('',*,*,#8205,.F.);
#10533=ORIENTED_EDGE('',*,*,#8195,.F.);
#10534=ORIENTED_EDGE('',*,*,#8205,.T.);
#10535=ORIENTED_EDGE('',*,*,#8202,.T.);
#10536=ORIENTED_EDGE('',*,*,#8199,.T.);
#10537=ORIENTED_EDGE('',*,*,#8196,.T.);
#10538=ORIENTED_EDGE('',*,*,#8204,.F.);
#10539=ORIENTED_EDGE('',*,*,#8194,.F.);
#10540=ORIENTED_EDGE('',*,*,#8198,.F.);
#10541=ORIENTED_EDGE('',*,*,#8201,.F.);
#12233=CYLINDRICAL_SURFACE('',#15336,0.164999999999999);
#12234=CYLINDRICAL_SURFACE('',#15341,0.604999999999997);
#12801=ADVANCED_FACE('',(#2434),#1845,.T.);
#12802=ADVANCED_FACE('',(#2435),#12233,.F.);
#12803=ADVANCED_FACE('',(#2436),#1846,.T.);
#12804=ADVANCED_FACE('',(#2437,#1454),#12234,.F.);
#12805=ADVANCED_FACE('',(#2438,#1455),#1847,.T.);
#12806=ADVANCED_FACE('',(#2439,#1456),#1848,.T.);
#12807=ADVANCED_FACE('',(#2440,#1457),#1849,.T.);
#12808=ADVANCED_FACE('',(#2441),#1850,.T.);
#12809=ADVANCED_FACE('',(#2442),#1851,.T.);
#12810=ADVANCED_FACE('',(#2443),#1852,.F.);
#13295=CLOSED_SHELL('',(#12801,#12802,#12803,#12804,#12805,#12806,#12807,
#12808,#12809,#12810));
#15333=AXIS2_PLACEMENT_3D('',#22687,#18396,#18397);
#15334=AXIS2_PLACEMENT_3D('',#22688,#18398,#18399);
#15335=AXIS2_PLACEMENT_3D('',#22692,#18401,#18402);
#15336=AXIS2_PLACEMENT_3D('',#22693,#18403,#18404);
#15337=AXIS2_PLACEMENT_3D('',#22710,#18405,#18406);
#15338=AXIS2_PLACEMENT_3D('',#22713,#18408,#18409);
#15339=AXIS2_PLACEMENT_3D('',#22715,#18410,#18411);
#15340=AXIS2_PLACEMENT_3D('',#22730,#18412,#18413);
#15341=AXIS2_PLACEMENT_3D('',#22732,#18415,#18416);
#15342=AXIS2_PLACEMENT_3D('',#22734,#18417,#18418);
#15343=AXIS2_PLACEMENT_3D('',#22737,#18420,#18421);
#15344=AXIS2_PLACEMENT_3D('',#22738,#18422,#18423);
#15345=AXIS2_PLACEMENT_3D('',#22747,#18428,#18429);
#15346=AXIS2_PLACEMENT_3D('',#22753,#18433,#18434);
#15347=AXIS2_PLACEMENT_3D('',#22759,#18438,#18439);
#15348=AXIS2_PLACEMENT_3D('',#22762,#18442,#18443);
#15349=AXIS2_PLACEMENT_3D('',#22763,#18444,#18445);
#18396=DIRECTION('axis',(0.,0.,1.));
#18397=DIRECTION('refdir',(1.,0.,0.));
#18398=DIRECTION('center_axis',(1.,0.,0.));
#18399=DIRECTION('ref_axis',(0.,0.,-1.));
#18400=DIRECTION('',(0.,1.,0.));
#18401=DIRECTION('center_axis',(1.,0.,0.));
#18402=DIRECTION('ref_axis',(0.,0.,-1.));
#18403=DIRECTION('center_axis',(1.,0.,0.));
#18404=DIRECTION('ref_axis',(0.,0.,-1.));
#18405=DIRECTION('center_axis',(1.,0.,0.));
#18406=DIRECTION('ref_axis',(0.,0.,-1.));
#18407=DIRECTION('',(1.,0.,0.));
#18408=DIRECTION('center_axis',(-1.,0.,0.));
#18409=DIRECTION('ref_axis',(0.,0.,-1.));
#18410=DIRECTION('center_axis',(1.,0.,0.));
#18411=DIRECTION('ref_axis',(0.,0.,-1.));
#18412=DIRECTION('center_axis',(1.,0.,0.));
#18413=DIRECTION('ref_axis',(0.,0.,-1.));
#18414=DIRECTION('',(0.,-1.,0.));
#18415=DIRECTION('center_axis',(0.,1.,0.));
#18416=DIRECTION('ref_axis',(1.,0.,0.));
#18417=DIRECTION('center_axis',(0.,1.,0.));
#18418=DIRECTION('ref_axis',(1.,0.,0.));
#18419=DIRECTION('',(0.,1.,0.));
#18420=DIRECTION('center_axis',(0.,-1.,0.));
#18421=DIRECTION('ref_axis',(1.,0.,0.));
#18422=DIRECTION('center_axis',(0.,1.,0.));
#18423=DIRECTION('ref_axis',(-1.,0.,0.));
#18424=DIRECTION('',(-1.,0.,0.));
#18425=DIRECTION('',(0.,0.,1.));
#18426=DIRECTION('',(-1.,0.,0.));
#18427=DIRECTION('',(0.,0.,1.));
#18428=DIRECTION('center_axis',(1.,0.,0.));
#18429=DIRECTION('ref_axis',(0.,1.,0.));
#18430=DIRECTION('',(0.,1.,0.));
#18431=DIRECTION('',(0.,1.,0.));
#18432=DIRECTION('',(0.,0.,1.));
#18433=DIRECTION('center_axis',(0.,-1.,0.));
#18434=DIRECTION('ref_axis',(1.,0.,0.));
#18435=DIRECTION('',(1.,0.,0.));
#18436=DIRECTION('',(1.,0.,0.));
#18437=DIRECTION('',(0.,0.,1.));
#18438=DIRECTION('center_axis',(-1.,0.,0.));
#18439=DIRECTION('ref_axis',(0.,-1.,0.));
#18440=DIRECTION('',(0.,-1.,0.));
#18441=DIRECTION('',(0.,-1.,0.));
#18442=DIRECTION('center_axis',(0.,0.,1.));
#18443=DIRECTION('ref_axis',(1.,0.,0.));
#18444=DIRECTION('center_axis',(0.,0.,1.));
#18445=DIRECTION('ref_axis',(1.,0.,0.));
#22687=CARTESIAN_POINT('',(0.,0.,0.));
#22688=CARTESIAN_POINT('Origin',(39.31983346,0.,13.));
#22689=CARTESIAN_POINT('',(39.31983346,-0.0964364949201854,12.8661157124697));
#22690=CARTESIAN_POINT('',(39.31983346,0.0964364949201854,12.8661157124697));
#22691=CARTESIAN_POINT('',(39.31983346,-3.6,12.8661157124697));
#22692=CARTESIAN_POINT('Origin',(39.31983346,0.,13.));
#22693=CARTESIAN_POINT('Origin',(39.31983346,0.,13.));
#22694=CARTESIAN_POINT('',(39.31983346,-0.0964364949201854,13.1338842875303));
#22695=CARTESIAN_POINT('Ctrl Pts',(39.31983346,-0.0964364949201853,13.1338842875303));
#22696=CARTESIAN_POINT('Ctrl Pts',(39.3210318640464,-0.103768349789616,
13.1286031720394));
#22697=CARTESIAN_POINT('Ctrl Pts',(39.3222741026686,-0.110552785281792,
13.1227924525098));
#22698=CARTESIAN_POINT('Ctrl Pts',(39.3263441031883,-0.1312614058317,13.1020838319599));
#22699=CARTESIAN_POINT('Ctrl Pts',(39.3293775570573,-0.143943476007901,
13.0836002135947));
#22700=CARTESIAN_POINT('Ctrl Pts',(39.3336505364571,-0.160815615633794,
13.0429774150043));
#22701=CARTESIAN_POINT('Ctrl Pts',(39.3348334620742,-0.164999999999999,
13.0208299403328));
#22702=CARTESIAN_POINT('Ctrl Pts',(39.3348334620742,-0.164999999999999,
12.9791700596672));
#22703=CARTESIAN_POINT('Ctrl Pts',(39.3336505364571,-0.160815615633794,
12.9570225849957));
#22704=CARTESIAN_POINT('Ctrl Pts',(39.3293775570573,-0.143943476007901,
12.9163997864053));
#22705=CARTESIAN_POINT('Ctrl Pts',(39.3263441031883,-0.1312614058317,12.8979161680401));
#22706=CARTESIAN_POINT('Ctrl Pts',(39.3222741026686,-0.110552785281793,
12.8772075474902));
#22707=CARTESIAN_POINT('Ctrl Pts',(39.3210318640464,-0.103768349789615,
12.8713968279606));
#22708=CARTESIAN_POINT('Ctrl Pts',(39.31983346,-0.0964364949201854,12.8661157124697));
#22709=CARTESIAN_POINT('',(39.31983346,-2.02066721859312E-17,13.165));
#22710=CARTESIAN_POINT('Origin',(39.31983346,0.,13.));
#22711=CARTESIAN_POINT('',(39.7298334620742,2.02066721859312E-17,13.165));
#22712=CARTESIAN_POINT('',(39.31983346,-2.02066721859312E-17,13.165));
#22713=CARTESIAN_POINT('Origin',(39.7298334620742,0.,13.));
#22714=CARTESIAN_POINT('',(39.31983346,0.0964364949201854,13.1338842875303));
#22715=CARTESIAN_POINT('Origin',(39.31983346,0.,13.));
#22716=CARTESIAN_POINT('Ctrl Pts',(39.31983346,0.0964364949201854,12.8661157124697));
#22717=CARTESIAN_POINT('Ctrl Pts',(39.3210318640464,0.103768349789616,12.8713968279606));
#22718=CARTESIAN_POINT('Ctrl Pts',(39.3222741026686,0.110552785281793,12.8772075474902));
#22719=CARTESIAN_POINT('Ctrl Pts',(39.3263441031883,0.1312614058317,12.8979161680401));
#22720=CARTESIAN_POINT('Ctrl Pts',(39.3293775570573,0.143943476007901,12.9163997864053));
#22721=CARTESIAN_POINT('Ctrl Pts',(39.3336505364571,0.160815615633794,12.9570225849957));
#22722=CARTESIAN_POINT('Ctrl Pts',(39.3348334620742,0.164999999999999,12.9791700596672));
#22723=CARTESIAN_POINT('Ctrl Pts',(39.3348334620742,0.164999999999999,13.0208299403328));
#22724=CARTESIAN_POINT('Ctrl Pts',(39.3336505364571,0.160815615633794,13.0429774150043));
#22725=CARTESIAN_POINT('Ctrl Pts',(39.3293775570573,0.143943476007901,13.0836002135947));
#22726=CARTESIAN_POINT('Ctrl Pts',(39.3263441031883,0.1312614058317,13.1020838319599));
#22727=CARTESIAN_POINT('Ctrl Pts',(39.3222741026686,0.110552785281792,13.1227924525098));
#22728=CARTESIAN_POINT('Ctrl Pts',(39.3210318640464,0.103768349789616,13.1286031720394));
#22729=CARTESIAN_POINT('Ctrl Pts',(39.31983346,0.0964364949201853,13.1338842875303));
#22730=CARTESIAN_POINT('Origin',(39.31983346,0.,13.));
#22731=CARTESIAN_POINT('',(39.31983346,-3.6,13.1338842875303));
#22732=CARTESIAN_POINT('Origin',(38.7298334620742,-3.6,13.));
#22733=CARTESIAN_POINT('',(38.1248334620742,-3.5,13.));
#22734=CARTESIAN_POINT('Origin',(38.7298334620742,-3.5,13.));
#22735=CARTESIAN_POINT('',(38.1248334620742,3.5,13.));
#22736=CARTESIAN_POINT('',(38.1248334620742,-3.6,13.));
#22737=CARTESIAN_POINT('Origin',(38.7298334620742,3.5,13.));
#22738=CARTESIAN_POINT('Origin',(39.7298334620742,3.5,12.));
#22739=CARTESIAN_POINT('',(39.7298334620742,3.5,12.));
#22740=CARTESIAN_POINT('',(37.7298334620742,3.5,12.));
#22741=CARTESIAN_POINT('',(39.7298334620742,3.5,12.));
#22742=CARTESIAN_POINT('',(37.7298334620742,3.5,14.3));
#22743=CARTESIAN_POINT('',(37.7298334620742,3.5,12.));
#22744=CARTESIAN_POINT('',(39.7298334620742,3.5,14.3));
#22745=CARTESIAN_POINT('',(39.7298334620742,3.5,14.3));
#22746=CARTESIAN_POINT('',(39.7298334620742,3.5,12.));
#22747=CARTESIAN_POINT('Origin',(39.7298334620742,-3.5,12.));
#22748=CARTESIAN_POINT('',(39.7298334620742,-3.5,12.));
#22749=CARTESIAN_POINT('',(39.7298334620742,-3.5,12.));
#22750=CARTESIAN_POINT('',(39.7298334620742,-3.5,14.3));
#22751=CARTESIAN_POINT('',(39.7298334620742,-3.5,14.3));
#22752=CARTESIAN_POINT('',(39.7298334620742,-3.5,12.));
#22753=CARTESIAN_POINT('Origin',(37.7298334620742,-3.5,12.));
#22754=CARTESIAN_POINT('',(37.7298334620742,-3.5,12.));
#22755=CARTESIAN_POINT('',(37.7298334620742,-3.5,12.));
#22756=CARTESIAN_POINT('',(37.7298334620742,-3.5,14.3));
#22757=CARTESIAN_POINT('',(37.7298334620742,-3.5,14.3));
#22758=CARTESIAN_POINT('',(37.7298334620742,-3.5,12.));
#22759=CARTESIAN_POINT('Origin',(37.7298334620742,3.5,12.));
#22760=CARTESIAN_POINT('',(37.7298334620742,3.5,12.));
#22761=CARTESIAN_POINT('',(37.7298334620742,3.5,14.3));
#22762=CARTESIAN_POINT('Origin',(38.7298334620742,0.,14.3));
#22763=CARTESIAN_POINT('Origin',(38.7298334620742,0.,12.));
#24909=UNCERTAINTY_MEASURE_WITH_UNIT(LENGTH_MEASURE(0.001),#25101,
'DISTANCE_ACCURACY_VALUE',
'Maximum model space distance between geometric entities at asserted c
onnectivities');
#24979=UNCERTAINTY_MEASURE_WITH_UNIT(LENGTH_MEASURE(0.001),#25101,
'DISTANCE_ACCURACY_VALUE',
'Maximum model space distance between geometric entities at asserted c
onnectivities');
#25030=(
GEOMETRIC_REPRESENTATION_CONTEXT(3)
GLOBAL_UNCERTAINTY_ASSIGNED_CONTEXT((#24909))
GLOBAL_UNIT_ASSIGNED_CONTEXT((#25101,#25103,#25104))
REPRESENTATION_CONTEXT('','3D')
);
#25100=(
GEOMETRIC_REPRESENTATION_CONTEXT(3)
GLOBAL_UNCERTAINTY_ASSIGNED_CONTEXT((#24979))
GLOBAL_UNIT_ASSIGNED_CONTEXT((#25101,#25103,#25104))
REPRESENTATION_CONTEXT('','3D')
);
#25101=(
LENGTH_UNIT()
NAMED_UNIT(*)
SI_UNIT(.CENTI.,.METRE.)
);
#25103=(
NAMED_UNIT(*)
PLANE_ANGLE_UNIT()
SI_UNIT($,.RADIAN.)
);
#25104=(
NAMED_UNIT(*)
SI_UNIT($,.STERADIAN.)
SOLID_ANGLE_UNIT()
);
#25155=SHAPE_DEFINITION_REPRESENTATION(#25275,#25560);
#25275=PRODUCT_DEFINITION_SHAPE('',$,#25681);
#25560=SHAPE_REPRESENTATION('',(#15333),#25030);
#25630=PRODUCT_DEFINITION_CONTEXT('part definition',#25992,'design');
#25681=PRODUCT_DEFINITION('Sliding pivot crosshead (1)',
'Sliding pivot crosshead (1)',#25801,#25630);
#25801=PRODUCT_DEFINITION_FORMATION('',$,#26044);
#25992=APPLICATION_CONTEXT(
'Core Data for Automotive Mechanical Design Process');
#25993=PRODUCT_CONTEXT('part definition',#25992,'mechanical');
#26044=PRODUCT('Sliding pivot crosshead (1)',
'Sliding pivot crosshead (1)','Sliding pivot crosshead (1)',(#25993));
#26199=COLOUR_RGB('Off White',0.89,0.88,0.83);
#26200=FILL_AREA_STYLE_COLOUR('',#26199);
#26201=FILL_AREA_STYLE('',(#26200));
#26202=SURFACE_STYLE_FILL_AREA(#26201);
#26203=SURFACE_SIDE_STYLE('',(#26202));
#26204=SURFACE_STYLE_USAGE(.BOTH.,#26203);
#26205=PRESENTATION_STYLE_ASSIGNMENT((#26204));
ENDSEC;
END-ISO-10303-21;
